ISO-10303-21;
HEADER;
/* Generated by software containing ST-Developer
 * from STEP Tools, Inc. (www.steptools.com) 
 */

FILE_DESCRIPTION(
/* description */ ('Drill jig with bushing plate'),
/* implementation_level */ '2;1');

FILE_NAME(
/* name */ 'Pin keeper (1).step',
/* time_stamp */ '2026-10-27T10:51:08-07:00',
/* author */ (''),
/* organization */ (''),
/* preprocessor_version */ 'ST-DEVELOPER v20.2',
/* originating_system */ 'Autodesk Translation Framework v15.17.0.0',
/* authorisation */ '');

FILE_SCHEMA (('AUTOMOTIVE_DESIGN { 1 0 10303 214 3 1 1 }'));
ENDSEC;

DATA;
#10=MECHANICAL_DESIGN_GEOMETRIC_PRESENTATION_REPRESENTATION('',(#234),#6638);
#186=SHAPE_REPRESENTATION_RELATIONSHIP('SRR','None',#6750,#210);
#210=ADVANCED_BREP_SHAPE_REPRESENTATION('',(#258),#6623);
#234=STYLED_ITEM('',(#6943),#258);
#258=MANIFOLD_SOLID_BREP('Body1',#3601);
#332=FACE_BOUND('',#879,.T.);
#333=FACE_BOUND('',#881,.T.);
#429=PLANE('',#4077);
#430=PLANE('',#4078);
#599=FACE_OUTER_BOUND('',#876,.T.);
#600=FACE_OUTER_BOUND('',#877,.T.);
#601=FACE_OUTER_BOUND('',#878,.T.);
#602=FACE_OUTER_BOUND('',#880,.T.);
#876=EDGE_LOOP('',(#2843,#2844,#2845,#2846));
#877=EDGE_LOOP('',(#2847,#2848,#2849,#2850));
#878=EDGE_LOOP('',(#2851));
#879=EDGE_LOOP('',(#2852));
#880=EDGE_LOOP('',(#2853));
#881=EDGE_LOOP('',(#2854));
#1153=LINE('',#6039,#1414);
#1154=LINE('',#6045,#1415);
#1414=VECTOR('',#4836,0.225);
#1415=VECTOR('',#4843,0.8);
#1630=CIRCLE('',#4072,0.225);
#1631=CIRCLE('',#4073,0.225);
#1632=CIRCLE('',#4075,0.8);
#1633=CIRCLE('',#4076,0.8);
#1856=VERTEX_POINT('',#6036);
#1857=VERTEX_POINT('',#6038);
#1858=VERTEX_POINT('',#6042);
#1859=VERTEX_POINT('',#6044);
#2209=EDGE_CURVE('',#1856,#1856,#1630,.T.);
#2210=EDGE_CURVE('',#1856,#1857,#1153,.T.);
#2211=EDGE_CURVE('',#1857,#1857,#1631,.T.);
#2212=EDGE_CURVE('',#1858,#1858,#1632,.T.);
#2213=EDGE_CURVE('',#1858,#1859,#1154,.T.);
#2214=EDGE_CURVE('',#1859,#1859,#1633,.T.);
#2843=ORIENTED_EDGE('',*,*,#2209,.F.);
#2844=ORIENTED_EDGE('',*,*,#2210,.T.);
#2845=ORIENTED_EDGE('',*,*,#2211,.T.);
#2846=ORIENTED_EDGE('',*,*,#2210,.F.);
#2847=ORIENTED_EDGE('',*,*,#2212,.F.);
#2848=ORIENTED_EDGE('',*,*,#2213,.T.);
#2849=ORIENTED_EDGE('',*,*,#2214,.T.);
#2850=ORIENTED_EDGE('',*,*,#2213,.F.);
#2851=ORIENTED_EDGE('',*,*,#2212,.T.);
#2852=ORIENTED_EDGE('',*,*,#2209,.T.);
#2853=ORIENTED_EDGE('',*,*,#2214,.F.);
#2854=ORIENTED_EDGE('',*,*,#2211,.F.);
#3338=CYLINDRICAL_SURFACE('',#4071,0.225);
#3339=CYLINDRICAL_SURFACE('',#4074,0.8);
#3474=ADVANCED_FACE('',(#599),#3338,.F.);
#3475=ADVANCED_FACE('',(#600),#3339,.T.);
#3476=ADVANCED_FACE('',(#601,#332),#429,.T.);
#3477=ADVANCED_FACE('',(#602,#333),#430,.F.);
#3601=CLOSED_SHELL('',(#3474,#3475,#3476,#3477));
#4070=AXIS2_PLACEMENT_3D('',#6034,#4830,#4831);
#4071=AXIS2_PLACEMENT_3D('',#6035,#4832,#4833);
#4072=AXIS2_PLACEMENT_3D('',#6037,#4834,#4835);
#4073=AXIS2_PLACEMENT_3D('',#6040,#4837,#4838);
#4074=AXIS2_PLACEMENT_3D('',#6041,#4839,#4840);
#4075=AXIS2_PLACEMENT_3D('',#6043,#4841,#4842);
#4076=AXIS2_PLACEMENT_3D('',#6046,#4844,#4845);
#4077=AXIS2_PLACEMENT_3D('',#6047,#4846,#4847);
#4078=AXIS2_PLACEMENT_3D('',#6048,#4848,#4849);
#4830=DIRECTION('axis',(0.,0.,1.));
#4831=DIRECTION('refdir',(1.,0.,0.));
#4832=DIRECTION('center_axis',(1.,0.,0.));
#4833=DIRECTION('ref_axis',(0.,0.,-1.));
#4834=DIRECTION('center_axis',(-1.,0.,0.));
#4835=DIRECTION('ref_axis',(0.,0.,-1.));
#4836=DIRECTION('',(-1.,0.,0.));
#4837=DIRECTION('center_axis',(-1.,0.,0.));
#4838=DIRECTION('ref_axis',(0.,0.,-1.));
#4839=DIRECTION('center_axis',(1.,0.,0.));
#4840=DIRECTION('ref_axis',(0.,0.,-1.));
#4841=DIRECTION('center_axis',(1.,0.,0.));
#4842=DIRECTION('ref_axis',(0.,0.,-1.));
#4843=DIRECTION('',(-1.,0.,0.));
#4844=DIRECTION('center_axis',(1.,0.,0.));
#4845=DIRECTION('ref_axis',(0.,0.,-1.));
#4846=DIRECTION('center_axis',(1.,0.,0.));
#4847=DIRECTION('ref_axis',(0.,0.,-1.));
#4848=DIRECTION('center_axis',(1.,0.,0.));
#4849=DIRECTION('ref_axis',(0.,0.,-1.));
#6034=CARTESIAN_POINT('',(0.,0.,0.));
#6035=CARTESIAN_POINT('Origin',(7.6,-6.,3.5));
#6036=CARTESIAN_POINT('',(7.8,-6.,3.725));
#6037=CARTESIAN_POINT('Origin',(7.8,-6.,3.5));
#6038=CARTESIAN_POINT('',(7.6,-6.,3.725));
#6039=CARTESIAN_POINT('',(7.6,-6.,3.725));
#6040=CARTESIAN_POINT('Origin',(7.6,-6.,3.5));
#6041=CARTESIAN_POINT('Origin',(7.6,-6.,3.5));
#6042=CARTESIAN_POINT('',(7.8,-6.,4.3));
#6043=CARTESIAN_POINT('Origin',(7.8,-6.,3.5));
#6044=CARTESIAN_POINT('',(7.6,-6.,4.3));
#6045=CARTESIAN_POINT('',(7.6,-6.,4.3));
#6046=CARTESIAN_POINT('Origin',(7.6,-6.,3.5));
#6047=CARTESIAN_POINT('Origin',(7.8,-6.,3.5));
#6048=CARTESIAN_POINT('Origin',(7.6,-6.,3.5));
#6594=UNCERTAINTY_MEASURE_WITH_UNIT(LENGTH_MEASURE(0.001),#6639,
'DISTANCE_ACCURACY_VALUE',
'Maximum model space distance between geometric entities at asserted c
onnectivities');
#6609=UNCERTAINTY_MEASURE_WITH_UNIT(LENGTH_MEASURE(0.001),#6639,
'DISTANCE_ACCURACY_VALUE',
'Maximum model space distance between geometric entities at asserted c
onnectivities');
#6623=(
GEOMETRIC_REPRESENTATION_CONTEXT(3)
GLOBAL_UNCERTAINTY_ASSIGNED_CONTEXT((#6594))
GLOBAL_UNIT_ASSIGNED_CONTEXT((#6639,#6641,#6642))
REPRESENTATION_CONTEXT('','3D')
);
#6638=(
GEOMETRIC_REPRESENTATION_CONTEXT(3)
GLOBAL_UNCERTAINTY_ASSIGNED_CONTEXT((#6609))
GLOBAL_UNIT_ASSIGNED_CONTEXT((#6639,#6641,#6642))
REPRESENTATION_CONTEXT('','3D')
);
#6639=(
LENGTH_UNIT()
NAMED_UNIT(*)
SI_UNIT(.CENTI.,.METRE.)
);
#6641=(
NAMED_UNIT(*)
PLANE_ANGLE_UNIT()
SI_UNIT($,.RADIAN.)
);
#6642=(
NAMED_UNIT(*)
SI_UNIT($,.STERADIAN.)
SOLID_ANGLE_UNIT()
);
#6656=SHAPE_DEFINITION_REPRESENTATION(#6684,#6750);
#6684=PRODUCT_DEFINITION_SHAPE('',$,#6779);
#6750=SHAPE_REPRESENTATION('',(#4070),#6623);
#6765=PRODUCT_DEFINITION_CONTEXT('part definition',#6851,'design');
#6779=PRODUCT_DEFINITION('Pin keeper (1)','Pin keeper (1)',#6807,#6765);
#6807=PRODUCT_DEFINITION_FORMATION('',$,#6866);
#6851=APPLICATION_CONTEXT(
'Core Data for Automotive Mechanical Design Process');
#6852=PRODUCT_CONTEXT('part definition',#6851,'mechanical');
#6866=PRODUCT('Pin keeper (1)','Pin keeper (1)','Pin keeper (1)',(#6852));
#6937=COLOUR_RGB('Grey',0.48,0.52,0.57);
#6938=FILL_AREA_STYLE_COLOUR('',#6937);
#6939=FILL_AREA_STYLE('',(#6938));
#6940=SURFACE_STYLE_FILL_AREA(#6939);
#6941=SURFACE_SIDE_STYLE('',(#6940));
#6942=SURFACE_STYLE_USAGE(.BOTH.,#6941);
#6943=PRESENTATION_STYLE_ASSIGNMENT((#6942));
ENDSEC;
END-ISO-10303-21;
